ISO-10303-21;
HEADER;
/* Generated by software containing ST-Developer
 * from STEP Tools, Inc. (www.steptools.com) 
 */

FILE_DESCRIPTION(
/* description */ ('Rotary union on bearing shaft'),
/* implementation_level */ '2;1');

FILE_NAME(
/* name */ 'Socket Set Screw - M5x8.step',
/* time_stamp */ '2026-10-28T03:24:01-07:00',
/* author */ (''),
/* organization */ (''),
/* preprocessor_version */ 'ST-DEVELOPER v20.2',
/* originating_system */ 'Autodesk Translation Framework v15.17.0.0',
/* authorisation */ '');

FILE_SCHEMA (('AUTOMOTIVE_DESIGN { 1 0 10303 214 3 1 1 }'));
ENDSEC;

DATA;
#10=MECHANICAL_DESIGN_GEOMETRIC_PRESENTATION_REPRESENTATION('',(#345),#9448);
#215=CONICAL_SURFACE('',#5773,0.235,0.785398163397448);
#216=CONICAL_SURFACE('',#5777,0.2125,0.785398163397448);
#283=SHAPE_REPRESENTATION_RELATIONSHIP('SRR','None',#9585,#310);
#310=ADVANCED_BREP_SHAPE_REPRESENTATION('',(#378),#9445);
#345=STYLED_ITEM('',(#9785),#378);
#378=MANIFOLD_SOLID_BREP('Body1',#4902);
#485=FACE_BOUND('',#1328,.T.);
#626=PLANE('',#5764);
#627=PLANE('',#5765);
#628=PLANE('',#5766);
#629=PLANE('',#5767);
#630=PLANE('',#5768);
#631=PLANE('',#5769);
#632=PLANE('',#5770);
#633=PLANE('',#5771);
#634=PLANE('',#5779);
#916=FACE_OUTER_BOUND('',#1320,.T.);
#917=FACE_OUTER_BOUND('',#1321,.T.);
#918=FACE_OUTER_BOUND('',#1322,.T.);
#919=FACE_OUTER_BOUND('',#1323,.T.);
#920=FACE_OUTER_BOUND('',#1324,.T.);
#921=FACE_OUTER_BOUND('',#1325,.T.);
#922=FACE_OUTER_BOUND('',#1326,.T.);
#923=FACE_OUTER_BOUND('',#1327,.T.);
#924=FACE_OUTER_BOUND('',#1329,.T.);
#925=FACE_OUTER_BOUND('',#1330,.T.);
#926=FACE_OUTER_BOUND('',#1331,.T.);
#927=FACE_OUTER_BOUND('',#1332,.T.);
#1320=EDGE_LOOP('',(#4317,#4318,#4319,#4320));
#1321=EDGE_LOOP('',(#4321,#4322,#4323,#4324));
#1322=EDGE_LOOP('',(#4325,#4326,#4327,#4328));
#1323=EDGE_LOOP('',(#4329,#4330,#4331,#4332));
#1324=EDGE_LOOP('',(#4333,#4334,#4335,#4336));
#1325=EDGE_LOOP('',(#4337,#4338,#4339,#4340));
#1326=EDGE_LOOP('',(#4341,#4342,#4343,#4344,#4345,#4346));
#1327=EDGE_LOOP('',(#4347));
#1328=EDGE_LOOP('',(#4348,#4349,#4350,#4351,#4352,#4353));
#1329=EDGE_LOOP('',(#4354,#4355,#4356,#4357));
#1330=EDGE_LOOP('',(#4358,#4359,#4360,#4361));
#1331=EDGE_LOOP('',(#4362,#4363,#4364,#4365));
#1332=EDGE_LOOP('',(#4366));
#1612=LINE('',#9203,#1932);
#1613=LINE('',#9205,#1933);
#1614=LINE('',#9207,#1934);
#1615=LINE('',#9208,#1935);
#1616=LINE('',#9211,#1936);
#1617=LINE('',#9213,#1937);
#1618=LINE('',#9214,#1938);
#1619=LINE('',#9217,#1939);
#1620=LINE('',#9219,#1940);
#1621=LINE('',#9220,#1941);
#1622=LINE('',#9223,#1942);
#1623=LINE('',#9225,#1943);
#1624=LINE('',#9226,#1944);
#1625=LINE('',#9229,#1945);
#1626=LINE('',#9231,#1946);
#1627=LINE('',#9232,#1947);
#1628=LINE('',#9234,#1948);
#1629=LINE('',#9235,#1949);
#1630=LINE('',#9243,#1950);
#1631=LINE('',#9247,#1951);
#1632=LINE('',#9251,#1952);
#1932=VECTOR('',#7201,1.);
#1933=VECTOR('',#7202,1.);
#1934=VECTOR('',#7203,1.);
#1935=VECTOR('',#7204,1.);
#1936=VECTOR('',#7207,1.);
#1937=VECTOR('',#7208,1.);
#1938=VECTOR('',#7209,1.);
#1939=VECTOR('',#7212,1.);
#1940=VECTOR('',#7213,1.);
#1941=VECTOR('',#7214,1.);
#1942=VECTOR('',#7217,1.);
#1943=VECTOR('',#7218,1.);
#1944=VECTOR('',#7219,1.);
#1945=VECTOR('',#7222,1.);
#1946=VECTOR('',#7223,1.);
#1947=VECTOR('',#7224,1.);
#1948=VECTOR('',#7227,1.);
#1949=VECTOR('',#7228,1.);
#1950=VECTOR('',#7239,0.235);
#1951=VECTOR('',#7244,0.25);
#1952=VECTOR('',#7249,0.2125);
#2241=CIRCLE('',#5772,0.22);
#2242=CIRCLE('',#5774,0.24505);
#2243=CIRCLE('',#5776,0.24505);
#2244=CIRCLE('',#5778,0.175);
#2609=VERTEX_POINT('',#9201);
#2610=VERTEX_POINT('',#9202);
#2611=VERTEX_POINT('',#9204);
#2612=VERTEX_POINT('',#9206);
#2613=VERTEX_POINT('',#9210);
#2614=VERTEX_POINT('',#9212);
#2615=VERTEX_POINT('',#9216);
#2616=VERTEX_POINT('',#9218);
#2617=VERTEX_POINT('',#9222);
#2618=VERTEX_POINT('',#9224);
#2619=VERTEX_POINT('',#9228);
#2620=VERTEX_POINT('',#9230);
#2621=VERTEX_POINT('',#9238);
#2622=VERTEX_POINT('',#9241);
#2623=VERTEX_POINT('',#9245);
#2624=VERTEX_POINT('',#9249);
#3186=EDGE_CURVE('',#2609,#2610,#1612,.T.);
#3187=EDGE_CURVE('',#2609,#2611,#1613,.T.);
#3188=EDGE_CURVE('',#2611,#2612,#1614,.T.);
#3189=EDGE_CURVE('',#2610,#2612,#1615,.T.);
#3190=EDGE_CURVE('',#2613,#2609,#1616,.T.);
#3191=EDGE_CURVE('',#2613,#2614,#1617,.T.);
#3192=EDGE_CURVE('',#2614,#2611,#1618,.T.);
#3193=EDGE_CURVE('',#2615,#2613,#1619,.T.);
#3194=EDGE_CURVE('',#2615,#2616,#1620,.T.);
#3195=EDGE_CURVE('',#2616,#2614,#1621,.T.);
#3196=EDGE_CURVE('',#2617,#2615,#1622,.T.);
#3197=EDGE_CURVE('',#2617,#2618,#1623,.T.);
#3198=EDGE_CURVE('',#2618,#2616,#1624,.T.);
#3199=EDGE_CURVE('',#2619,#2617,#1625,.T.);
#3200=EDGE_CURVE('',#2619,#2620,#1626,.T.);
#3201=EDGE_CURVE('',#2620,#2618,#1627,.T.);
#3202=EDGE_CURVE('',#2610,#2619,#1628,.T.);
#3203=EDGE_CURVE('',#2612,#2620,#1629,.T.);
#3204=EDGE_CURVE('',#2621,#2621,#2241,.T.);
#3205=EDGE_CURVE('',#2622,#2622,#2242,.T.);
#3206=EDGE_CURVE('',#2622,#2621,#1630,.T.);
#3207=EDGE_CURVE('',#2623,#2623,#2243,.F.);
#3208=EDGE_CURVE('',#2623,#2622,#1631,.T.);
#3209=EDGE_CURVE('',#2624,#2624,#2244,.T.);
#3210=EDGE_CURVE('',#2624,#2623,#1632,.T.);
#4317=ORIENTED_EDGE('',*,*,#3186,.F.);
#4318=ORIENTED_EDGE('',*,*,#3187,.T.);
#4319=ORIENTED_EDGE('',*,*,#3188,.T.);
#4320=ORIENTED_EDGE('',*,*,#3189,.F.);
#4321=ORIENTED_EDGE('',*,*,#3190,.F.);
#4322=ORIENTED_EDGE('',*,*,#3191,.T.);
#4323=ORIENTED_EDGE('',*,*,#3192,.T.);
#4324=ORIENTED_EDGE('',*,*,#3187,.F.);
#4325=ORIENTED_EDGE('',*,*,#3193,.F.);
#4326=ORIENTED_EDGE('',*,*,#3194,.T.);
#4327=ORIENTED_EDGE('',*,*,#3195,.T.);
#4328=ORIENTED_EDGE('',*,*,#3191,.F.);
#4329=ORIENTED_EDGE('',*,*,#3196,.F.);
#4330=ORIENTED_EDGE('',*,*,#3197,.T.);
#4331=ORIENTED_EDGE('',*,*,#3198,.T.);
#4332=ORIENTED_EDGE('',*,*,#3194,.F.);
#4333=ORIENTED_EDGE('',*,*,#3199,.F.);
#4334=ORIENTED_EDGE('',*,*,#3200,.T.);
#4335=ORIENTED_EDGE('',*,*,#3201,.T.);
#4336=ORIENTED_EDGE('',*,*,#3197,.F.);
#4337=ORIENTED_EDGE('',*,*,#3202,.F.);
#4338=ORIENTED_EDGE('',*,*,#3189,.T.);
#4339=ORIENTED_EDGE('',*,*,#3203,.T.);
#4340=ORIENTED_EDGE('',*,*,#3200,.F.);
#4341=ORIENTED_EDGE('',*,*,#3203,.F.);
#4342=ORIENTED_EDGE('',*,*,#3188,.F.);
#4343=ORIENTED_EDGE('',*,*,#3192,.F.);
#4344=ORIENTED_EDGE('',*,*,#3195,.F.);
#4345=ORIENTED_EDGE('',*,*,#3198,.F.);
#4346=ORIENTED_EDGE('',*,*,#3201,.F.);
#4347=ORIENTED_EDGE('',*,*,#3204,.F.);
#4348=ORIENTED_EDGE('',*,*,#3186,.T.);
#4349=ORIENTED_EDGE('',*,*,#3202,.T.);
#4350=ORIENTED_EDGE('',*,*,#3199,.T.);
#4351=ORIENTED_EDGE('',*,*,#3196,.T.);
#4352=ORIENTED_EDGE('',*,*,#3193,.T.);
#4353=ORIENTED_EDGE('',*,*,#3190,.T.);
#4354=ORIENTED_EDGE('',*,*,#3205,.F.);
#4355=ORIENTED_EDGE('',*,*,#3206,.T.);
#4356=ORIENTED_EDGE('',*,*,#3204,.T.);
#4357=ORIENTED_EDGE('',*,*,#3206,.F.);
#4358=ORIENTED_EDGE('',*,*,#3207,.F.);
#4359=ORIENTED_EDGE('',*,*,#3208,.T.);
#4360=ORIENTED_EDGE('',*,*,#3205,.T.);
#4361=ORIENTED_EDGE('',*,*,#3208,.F.);
#4362=ORIENTED_EDGE('',*,*,#3209,.F.);
#4363=ORIENTED_EDGE('',*,*,#3210,.T.);
#4364=ORIENTED_EDGE('',*,*,#3207,.T.);
#4365=ORIENTED_EDGE('',*,*,#3210,.F.);
#4366=ORIENTED_EDGE('',*,*,#3209,.T.);
#4566=CYLINDRICAL_SURFACE('',#5775,0.24505);
#4829=ADVANCED_FACE('',(#916),#626,.F.);
#4830=ADVANCED_FACE('',(#917),#627,.F.);
#4831=ADVANCED_FACE('',(#918),#628,.F.);
#4832=ADVANCED_FACE('',(#919),#629,.F.);
#4833=ADVANCED_FACE('',(#920),#630,.F.);
#4834=ADVANCED_FACE('',(#921),#631,.F.);
#4835=ADVANCED_FACE('',(#922),#632,.F.);
#4836=ADVANCED_FACE('',(#923,#485),#633,.T.);
#4837=ADVANCED_FACE('',(#924),#215,.T.);
#4838=ADVANCED_FACE('',(#925),#4566,.T.);
#4839=ADVANCED_FACE('',(#926),#216,.T.);
#4840=ADVANCED_FACE('',(#927),#634,.T.);
#4902=CLOSED_SHELL('',(#4829,#4830,#4831,#4832,#4833,#4834,#4835,#4836,
#4837,#4838,#4839,#4840));
#5763=AXIS2_PLACEMENT_3D('',#9199,#7197,#7198);
#5764=AXIS2_PLACEMENT_3D('',#9200,#7199,#7200);
#5765=AXIS2_PLACEMENT_3D('',#9209,#7205,#7206);
#5766=AXIS2_PLACEMENT_3D('',#9215,#7210,#7211);
#5767=AXIS2_PLACEMENT_3D('',#9221,#7215,#7216);
#5768=AXIS2_PLACEMENT_3D('',#9227,#7220,#7221);
#5769=AXIS2_PLACEMENT_3D('',#9233,#7225,#7226);
#5770=AXIS2_PLACEMENT_3D('',#9236,#7229,#7230);
#5771=AXIS2_PLACEMENT_3D('',#9237,#7231,#7232);
#5772=AXIS2_PLACEMENT_3D('',#9239,#7233,#7234);
#5773=AXIS2_PLACEMENT_3D('',#9240,#7235,#7236);
#5774=AXIS2_PLACEMENT_3D('',#9242,#7237,#7238);
#5775=AXIS2_PLACEMENT_3D('',#9244,#7240,#7241);
#5776=AXIS2_PLACEMENT_3D('',#9246,#7242,#7243);
#5777=AXIS2_PLACEMENT_3D('',#9248,#7245,#7246);
#5778=AXIS2_PLACEMENT_3D('',#9250,#7247,#7248);
#5779=AXIS2_PLACEMENT_3D('',#9252,#7250,#7251);
#7197=DIRECTION('axis',(0.,0.,1.));
#7198=DIRECTION('refdir',(1.,0.,0.));
#7199=DIRECTION('center_axis',(0.866025403784439,0.,-0.5));
#7200=DIRECTION('ref_axis',(0.5,0.,0.866025403784439));
#7201=DIRECTION('',(0.5,0.,0.866025403784439));
#7202=DIRECTION('',(0.,-1.,0.));
#7203=DIRECTION('',(0.5,0.,0.866025403784439));
#7204=DIRECTION('',(0.,-1.,0.));
#7205=DIRECTION('center_axis',(1.92296268638356E-16,0.,-1.));
#7206=DIRECTION('ref_axis',(1.,0.,1.92296268638356E-16));
#7207=DIRECTION('',(1.,0.,1.92296268638356E-16));
#7208=DIRECTION('',(0.,-1.,0.));
#7209=DIRECTION('',(1.,0.,1.92296268638356E-16));
#7210=DIRECTION('center_axis',(-0.866025403784439,0.,-0.5));
#7211=DIRECTION('ref_axis',(0.5,0.,-0.866025403784439));
#7212=DIRECTION('',(0.5,0.,-0.866025403784439));
#7213=DIRECTION('',(0.,-1.,0.));
#7214=DIRECTION('',(0.5,0.,-0.866025403784438));
#7215=DIRECTION('center_axis',(-0.866025403784439,0.,0.5));
#7216=DIRECTION('ref_axis',(-0.5,0.,-0.866025403784439));
#7217=DIRECTION('',(-0.5,0.,-0.866025403784439));
#7218=DIRECTION('',(0.,-1.,0.));
#7219=DIRECTION('',(-0.5,0.,-0.866025403784439));
#7220=DIRECTION('center_axis',(-1.92296268638356E-16,0.,1.));
#7221=DIRECTION('ref_axis',(-1.,0.,-1.92296268638356E-16));
#7222=DIRECTION('',(-1.,0.,-1.92296268638356E-16));
#7223=DIRECTION('',(0.,-1.,0.));
#7224=DIRECTION('',(-1.,0.,-1.92296268638356E-16));
#7225=DIRECTION('center_axis',(0.866025403784439,0.,0.5));
#7226=DIRECTION('ref_axis',(-0.5,0.,0.866025403784439));
#7227=DIRECTION('',(-0.5,0.,0.866025403784439));
#7228=DIRECTION('',(-0.5,0.,0.866025403784439));
#7229=DIRECTION('center_axis',(0.,-1.,0.));
#7230=DIRECTION('ref_axis',(0.,0.,-1.));
#7231=DIRECTION('center_axis',(0.,1.,0.));
#7232=DIRECTION('ref_axis',(0.,0.,1.));
#7233=DIRECTION('center_axis',(0.,-1.,0.));
#7234=DIRECTION('ref_axis',(1.,0.,0.));
#7235=DIRECTION('center_axis',(0.,-1.,0.));
#7236=DIRECTION('ref_axis',(1.,0.,0.));
#7237=DIRECTION('center_axis',(0.,-1.,0.));
#7238=DIRECTION('ref_axis',(1.,0.,0.));
#7239=DIRECTION('',(0.707106781186547,0.707106781186548,8.65956056235493E-17));
#7240=DIRECTION('center_axis',(0.,-1.,0.));
#7241=DIRECTION('ref_axis',(1.,0.,0.));
#7242=DIRECTION('center_axis',(0.,1.,0.));
#7243=DIRECTION('ref_axis',(1.,0.,0.));
#7244=DIRECTION('',(0.,1.,0.));
#7245=DIRECTION('center_axis',(0.,1.,0.));
#7246=DIRECTION('ref_axis',(1.,0.,0.));
#7247=DIRECTION('center_axis',(0.,-1.,0.));
#7248=DIRECTION('ref_axis',(1.,0.,0.));
#7249=DIRECTION('',(-0.707106781186547,0.707106781186548,-8.65956056235493E-17));
#7250=DIRECTION('center_axis',(0.,-1.,0.));
#7251=DIRECTION('ref_axis',(0.,0.,-1.));
#9199=CARTESIAN_POINT('',(0.,0.,0.));
#9200=CARTESIAN_POINT('Origin',(0.0721687836487032,0.,-0.125));
#9201=CARTESIAN_POINT('',(0.0721687836487032,0.,-0.125));
#9202=CARTESIAN_POINT('',(0.144337567297406,0.,0.));
#9203=CARTESIAN_POINT('',(0.117710979560879,0.,-0.0461186027918559));
#9204=CARTESIAN_POINT('',(0.0721687836487032,-0.25,-0.125));
#9205=CARTESIAN_POINT('',(0.0721687836487032,0.,-0.125));
#9206=CARTESIAN_POINT('',(0.144337567297406,-0.25,0.));
#9207=CARTESIAN_POINT('',(0.144337567297406,-0.25,0.));
#9208=CARTESIAN_POINT('',(0.144337567297406,0.,0.));
#9209=CARTESIAN_POINT('Origin',(-0.0721687836487032,0.,-0.125));
#9210=CARTESIAN_POINT('',(-0.0721687836487032,0.,-0.125));
#9211=CARTESIAN_POINT('',(0.0739156081756484,0.,-0.125));
#9212=CARTESIAN_POINT('',(-0.0721687836487032,-0.25,-0.125));
#9213=CARTESIAN_POINT('',(-0.0721687836487032,0.,-0.125));
#9214=CARTESIAN_POINT('',(0.0721687836487032,-0.25,-0.125));
#9215=CARTESIAN_POINT('Origin',(-0.144337567297406,0.,-4.16333634234434E-17));
#9216=CARTESIAN_POINT('',(-0.144337567297406,0.,-1.76762539787485E-17));
#9217=CARTESIAN_POINT('',(-0.0987953713852306,0.,-0.0788813972081442));
#9218=CARTESIAN_POINT('',(-0.144337567297406,-0.25,-2.77555756156289E-17));
#9219=CARTESIAN_POINT('',(-0.144337567297406,0.,-1.76762539787485E-17));
#9220=CARTESIAN_POINT('',(-0.0721687836487032,-0.25,-0.125));
#9221=CARTESIAN_POINT('Origin',(-0.0721687836487033,0.,0.125));
#9222=CARTESIAN_POINT('',(-0.0721687836487033,0.,0.125));
#9223=CARTESIAN_POINT('',(-0.0627109795608791,0.,0.141381397208144));
#9224=CARTESIAN_POINT('',(-0.0721687836487033,-0.25,0.125));
#9225=CARTESIAN_POINT('',(-0.0721687836487033,0.,0.125));
#9226=CARTESIAN_POINT('',(-0.144337567297406,-0.25,-1.76762539787485E-17));
#9227=CARTESIAN_POINT('Origin',(0.0721687836487032,0.,0.125));
#9228=CARTESIAN_POINT('',(0.0721687836487032,0.,0.125));
#9229=CARTESIAN_POINT('',(0.146084391824352,0.,0.125));
#9230=CARTESIAN_POINT('',(0.0721687836487032,-0.25,0.125));
#9231=CARTESIAN_POINT('',(0.0721687836487032,0.,0.125));
#9232=CARTESIAN_POINT('',(-0.0721687836487033,-0.25,0.125));
#9233=CARTESIAN_POINT('Origin',(0.144337567297406,0.,0.));
#9234=CARTESIAN_POINT('',(0.153795371385231,0.,-0.0163813972081441));
#9235=CARTESIAN_POINT('',(0.0721687836487032,-0.25,0.125));
#9236=CARTESIAN_POINT('Origin',(0.,-0.25,0.));
#9237=CARTESIAN_POINT('Origin',(0.22,0.,0.));
#9238=CARTESIAN_POINT('',(-0.22,-8.67361737988404E-18,-2.69422295812418E-17));
#9239=CARTESIAN_POINT('Origin',(0.,0.,0.));
#9240=CARTESIAN_POINT('Origin',(0.,-0.015,0.));
#9241=CARTESIAN_POINT('',(-0.24505,-0.02505,-3.00099698131059E-17));
#9242=CARTESIAN_POINT('Origin',(0.,-0.02505,0.));
#9243=CARTESIAN_POINT('',(-0.235,-0.015,-2.87791997799628E-17));
#9244=CARTESIAN_POINT('Origin',(0.,-0.3775,0.));
#9245=CARTESIAN_POINT('',(-0.24505,-0.72995,3.00099698131059E-17));
#9246=CARTESIAN_POINT('Origin',(0.,-0.72995,0.));
#9247=CARTESIAN_POINT('',(-0.24505,-0.3775,-3.00099698131059E-17));
#9248=CARTESIAN_POINT('Origin',(0.,-0.7625,0.));
#9249=CARTESIAN_POINT('',(-0.175,-0.8,-2.14313189850787E-17));
#9250=CARTESIAN_POINT('Origin',(0.,-0.8,0.));
#9251=CARTESIAN_POINT('',(-0.2125,-0.7625,-2.60237444818813E-17));
#9252=CARTESIAN_POINT('Origin',(0.,-0.8,0.));
#9413=UNCERTAINTY_MEASURE_WITH_UNIT(LENGTH_MEASURE(0.001),#9449,
'DISTANCE_ACCURACY_VALUE',
'Maximum model space distance between geometric entities at asserted c
onnectivities');
#9416=UNCERTAINTY_MEASURE_WITH_UNIT(LENGTH_MEASURE(0.001),#9449,
'DISTANCE_ACCURACY_VALUE',
'Maximum model space distance between geometric entities at asserted c
onnectivities');
#9445=(
GEOMETRIC_REPRESENTATION_CONTEXT(3)
GLOBAL_UNCERTAINTY_ASSIGNED_CONTEXT((#9413))
GLOBAL_UNIT_ASSIGNED_CONTEXT((#9449,#9451,#9452))
REPRESENTATION_CONTEXT('','3D')
);
#9448=(
GEOMETRIC_REPRESENTATION_CONTEXT(3)
GLOBAL_UNCERTAINTY_ASSIGNED_CONTEXT((#9416))
GLOBAL_UNIT_ASSIGNED_CONTEXT((#9449,#9451,#9452))
REPRESENTATION_CONTEXT('','3D')
);
#9449=(
LENGTH_UNIT()
NAMED_UNIT(*)
SI_UNIT(.CENTI.,.METRE.)
);
#9451=(
NAMED_UNIT(*)
PLANE_ANGLE_UNIT()
SI_UNIT($,.RADIAN.)
);
#9452=(
NAMED_UNIT(*)
SI_UNIT($,.STERADIAN.)
SOLID_ANGLE_UNIT()
);
#9481=SHAPE_DEFINITION_REPRESENTATION(#9543,#9585);
#9543=PRODUCT_DEFINITION_SHAPE('',$,#9617);
#9585=SHAPE_REPRESENTATION('',(#5763),#9445);
#9588=PRODUCT_DEFINITION_CONTEXT('part definition',#9683,'design');
#9617=PRODUCT_DEFINITION('Socket Set Screw - M5x8',
'Socket Set Screw - M5x8',#9648,#9588);
#9648=PRODUCT_DEFINITION_FORMATION('',$,#9713);
#9683=APPLICATION_CONTEXT(
'Core Data for Automotive Mechanical Design Process');
#9684=PRODUCT_CONTEXT('part definition',#9683,'mechanical');
#9713=PRODUCT('Socket Set Screw - M5x8','Socket Set Screw - M5x8',
'Socket Set Screw - M5x8',(#9684));
#9779=COLOUR_RGB('Black',0.12,0.14,0.17);
#9780=FILL_AREA_STYLE_COLOUR('',#9779);
#9781=FILL_AREA_STYLE('',(#9780));
#9782=SURFACE_STYLE_FILL_AREA(#9781);
#9783=SURFACE_SIDE_STYLE('',(#9782));
#9784=SURFACE_STYLE_USAGE(.BOTH.,#9783);
#9785=PRESENTATION_STYLE_ASSIGNMENT((#9784));
ENDSEC;
END-ISO-10303-21;
